ISO-10303-21;
HEADER;
/* Generated by software containing ST-Developer
 * from STEP Tools, Inc. (www.steptools.com) 
 */

FILE_DESCRIPTION(
/* description */ ('Single-Axis Profile-Rail Linear Slide'),
/* implementation_level */ '2;1');

FILE_NAME(
/* name */ 'M5x14 Cap Screw.step',
/* time_stamp */ '2026-10-27T10:47:43-07:00',
/* author */ (''),
/* organization */ (''),
/* preprocessor_version */ 'ST-DEVELOPER v20.2',
/* originating_system */ 'Autodesk Translation Framework v15.17.0.0',
/* authorisation */ '');

FILE_SCHEMA (('AUTOMOTIVE_DESIGN { 1 0 10303 214 3 1 1 }'));
ENDSEC;

DATA;
#10=MECHANICAL_DESIGN_GEOMETRIC_PRESENTATION_REPRESENTATION('',(#342),#14478);
#243=CONICAL_SURFACE('',#9310,0.4,0.785398163397448);
#244=CONICAL_SURFACE('',#9314,0.41,0.785398163397448);
#245=CONICAL_SURFACE('',#9318,0.26,0.463647609000806);
#263=ORIENTED_CLOSED_SHELL('',*,#8602,.F.);
#268=BREP_WITH_VOIDS('Body1',#8603,(#263));
#288=SHAPE_REPRESENTATION_RELATIONSHIP('SRR','None',#14618,#315);
#315=ADVANCED_BREP_SHAPE_REPRESENTATION('',(#268),#14462);
#342=STYLED_ITEM('',(#14838),#268);
#437=FACE_BOUND('',#1659,.T.);
#725=PLANE('',#9298);
#726=PLANE('',#9299);
#727=PLANE('',#9300);
#728=PLANE('',#9301);
#729=PLANE('',#9302);
#730=PLANE('',#9303);
#731=PLANE('',#9304);
#732=PLANE('',#9305);
#733=PLANE('',#9306);
#734=PLANE('',#9308);
#735=PLANE('',#9316);
#1131=FACE_OUTER_BOUND('',#1645,.T.);
#1132=FACE_OUTER_BOUND('',#1646,.T.);
#1133=FACE_OUTER_BOUND('',#1647,.T.);
#1134=FACE_OUTER_BOUND('',#1648,.T.);
#1135=FACE_OUTER_BOUND('',#1649,.T.);
#1136=FACE_OUTER_BOUND('',#1650,.T.);
#1137=FACE_OUTER_BOUND('',#1651,.T.);
#1138=FACE_OUTER_BOUND('',#1652,.T.);
#1139=FACE_OUTER_BOUND('',#1653,.T.);
#1140=FACE_OUTER_BOUND('',#1654,.T.);
#1141=FACE_OUTER_BOUND('',#1655,.T.);
#1142=FACE_OUTER_BOUND('',#1656,.T.);
#1143=FACE_OUTER_BOUND('',#1657,.T.);
#1144=FACE_OUTER_BOUND('',#1658,.T.);
#1145=FACE_OUTER_BOUND('',#1660,.T.);
#1146=FACE_OUTER_BOUND('',#1661,.T.);
#1645=EDGE_LOOP('',(#7361,#7362,#7363,#7364));
#1646=EDGE_LOOP('',(#7365,#7366,#7367,#7368));
#1647=EDGE_LOOP('',(#7369,#7370,#7371,#7372));
#1648=EDGE_LOOP('',(#7373,#7374,#7375,#7376));
#1649=EDGE_LOOP('',(#7377,#7378,#7379,#7380));
#1650=EDGE_LOOP('',(#7381,#7382,#7383,#7384));
#1651=EDGE_LOOP('',(#7385,#7386,#7387,#7388,#7389,#7390));
#1652=EDGE_LOOP('',(#7391,#7392,#7393,#7394,#7395,#7396));
#1653=EDGE_LOOP('',(#7397));
#1654=EDGE_LOOP('',(#7398));
#1655=EDGE_LOOP('',(#7399,#7400,#7401,#7402));
#1656=EDGE_LOOP('',(#7403,#7404,#7405,#7406));
#1657=EDGE_LOOP('',(#7407,#7408,#7409,#7410));
#1658=EDGE_LOOP('',(#7411));
#1659=EDGE_LOOP('',(#7412));
#1660=EDGE_LOOP('',(#7413,#7414,#7415,#7416));
#1661=EDGE_LOOP('',(#7417,#7418,#7419,#7420));
#2542=LINE('',#13596,#3513);
#2543=LINE('',#13598,#3514);
#2544=LINE('',#13600,#3515);
#2545=LINE('',#13601,#3516);
#2546=LINE('',#13604,#3517);
#2547=LINE('',#13606,#3518);
#2548=LINE('',#13607,#3519);
#2549=LINE('',#13610,#3520);
#2550=LINE('',#13612,#3521);
#2551=LINE('',#13613,#3522);
#2552=LINE('',#13616,#3523);
#2553=LINE('',#13618,#3524);
#2554=LINE('',#13619,#3525);
#2555=LINE('',#13622,#3526);
#2556=LINE('',#13624,#3527);
#2557=LINE('',#13625,#3528);
#2558=LINE('',#13627,#3529);
#2559=LINE('',#13628,#3530);
#2560=LINE('',#13640,#3531);
#2561=LINE('',#13644,#3532);
#2562=LINE('',#13648,#3533);
#2563=LINE('',#13655,#3534);
#2564=LINE('',#13657,#3535);
#3513=VECTOR('',#11083,1.);
#3514=VECTOR('',#11084,1.);
#3515=VECTOR('',#11085,1.);
#3516=VECTOR('',#11086,1.);
#3517=VECTOR('',#11089,1.);
#3518=VECTOR('',#11090,1.);
#3519=VECTOR('',#11091,1.);
#3520=VECTOR('',#11094,1.);
#3521=VECTOR('',#11095,1.);
#3522=VECTOR('',#11096,1.);
#3523=VECTOR('',#11099,1.);
#3524=VECTOR('',#11100,1.);
#3525=VECTOR('',#11101,1.);
#3526=VECTOR('',#11104,1.);
#3527=VECTOR('',#11105,1.);
#3528=VECTOR('',#11106,1.);
#3529=VECTOR('',#11109,1.);
#3530=VECTOR('',#11110,1.);
#3531=VECTOR('',#11127,0.4);
#3532=VECTOR('',#11132,0.425);
#3533=VECTOR('',#11137,0.41);
#3534=VECTOR('',#11146,0.26);
#3535=VECTOR('',#11149,0.25);
#3852=CIRCLE('',#9307,0.24505);
#3853=CIRCLE('',#9309,0.375);
#3854=CIRCLE('',#9311,0.425);
#3855=CIRCLE('',#9313,0.425);
#3856=CIRCLE('',#9315,0.395);
#3857=CIRCLE('',#9317,0.27);
#3858=CIRCLE('',#9319,0.24505);
#4454=VERTEX_POINT('',#13594);
#4455=VERTEX_POINT('',#13595);
#4456=VERTEX_POINT('',#13597);
#4457=VERTEX_POINT('',#13599);
#4458=VERTEX_POINT('',#13603);
#4459=VERTEX_POINT('',#13605);
#4460=VERTEX_POINT('',#13609);
#4461=VERTEX_POINT('',#13611);
#4462=VERTEX_POINT('',#13615);
#4463=VERTEX_POINT('',#13617);
#4464=VERTEX_POINT('',#13621);
#4465=VERTEX_POINT('',#13623);
#4466=VERTEX_POINT('',#13632);
#4467=VERTEX_POINT('',#13635);
#4468=VERTEX_POINT('',#13638);
#4469=VERTEX_POINT('',#13642);
#4470=VERTEX_POINT('',#13646);
#4471=VERTEX_POINT('',#13650);
#4472=VERTEX_POINT('',#13653);
#5458=EDGE_CURVE('',#4454,#4455,#2542,.T.);
#5459=EDGE_CURVE('',#4455,#4456,#2543,.T.);
#5460=EDGE_CURVE('',#4456,#4457,#2544,.T.);
#5461=EDGE_CURVE('',#4454,#4457,#2545,.T.);
#5462=EDGE_CURVE('',#4455,#4458,#2546,.T.);
#5463=EDGE_CURVE('',#4458,#4459,#2547,.T.);
#5464=EDGE_CURVE('',#4459,#4456,#2548,.T.);
#5465=EDGE_CURVE('',#4458,#4460,#2549,.T.);
#5466=EDGE_CURVE('',#4460,#4461,#2550,.T.);
#5467=EDGE_CURVE('',#4461,#4459,#2551,.T.);
#5468=EDGE_CURVE('',#4460,#4462,#2552,.T.);
#5469=EDGE_CURVE('',#4462,#4463,#2553,.T.);
#5470=EDGE_CURVE('',#4463,#4461,#2554,.T.);
#5471=EDGE_CURVE('',#4462,#4464,#2555,.T.);
#5472=EDGE_CURVE('',#4464,#4465,#2556,.T.);
#5473=EDGE_CURVE('',#4465,#4463,#2557,.T.);
#5474=EDGE_CURVE('',#4464,#4454,#2558,.T.);
#5475=EDGE_CURVE('',#4457,#4465,#2559,.T.);
#5476=EDGE_CURVE('',#4466,#4466,#3852,.T.);
#5477=EDGE_CURVE('',#4467,#4467,#3853,.T.);
#5478=EDGE_CURVE('',#4468,#4468,#3854,.T.);
#5479=EDGE_CURVE('',#4468,#4467,#2560,.T.);
#5480=EDGE_CURVE('',#4469,#4469,#3855,.T.);
#5481=EDGE_CURVE('',#4469,#4468,#2561,.T.);
#5482=EDGE_CURVE('',#4470,#4470,#3856,.T.);
#5483=EDGE_CURVE('',#4470,#4469,#2562,.T.);
#5484=EDGE_CURVE('',#4471,#4471,#3857,.T.);
#5485=EDGE_CURVE('',#4472,#4472,#3858,.F.);
#5486=EDGE_CURVE('',#4472,#4471,#2563,.T.);
#5487=EDGE_CURVE('',#4466,#4472,#2564,.T.);
#7361=ORIENTED_EDGE('',*,*,#5458,.T.);
#7362=ORIENTED_EDGE('',*,*,#5459,.T.);
#7363=ORIENTED_EDGE('',*,*,#5460,.T.);
#7364=ORIENTED_EDGE('',*,*,#5461,.F.);
#7365=ORIENTED_EDGE('',*,*,#5462,.T.);
#7366=ORIENTED_EDGE('',*,*,#5463,.T.);
#7367=ORIENTED_EDGE('',*,*,#5464,.T.);
#7368=ORIENTED_EDGE('',*,*,#5459,.F.);
#7369=ORIENTED_EDGE('',*,*,#5465,.T.);
#7370=ORIENTED_EDGE('',*,*,#5466,.T.);
#7371=ORIENTED_EDGE('',*,*,#5467,.T.);
#7372=ORIENTED_EDGE('',*,*,#5463,.F.);
#7373=ORIENTED_EDGE('',*,*,#5468,.T.);
#7374=ORIENTED_EDGE('',*,*,#5469,.T.);
#7375=ORIENTED_EDGE('',*,*,#5470,.T.);
#7376=ORIENTED_EDGE('',*,*,#5466,.F.);
#7377=ORIENTED_EDGE('',*,*,#5471,.T.);
#7378=ORIENTED_EDGE('',*,*,#5472,.T.);
#7379=ORIENTED_EDGE('',*,*,#5473,.T.);
#7380=ORIENTED_EDGE('',*,*,#5469,.F.);
#7381=ORIENTED_EDGE('',*,*,#5474,.T.);
#7382=ORIENTED_EDGE('',*,*,#5461,.T.);
#7383=ORIENTED_EDGE('',*,*,#5475,.T.);
#7384=ORIENTED_EDGE('',*,*,#5472,.F.);
#7385=ORIENTED_EDGE('',*,*,#5474,.F.);
#7386=ORIENTED_EDGE('',*,*,#5471,.F.);
#7387=ORIENTED_EDGE('',*,*,#5468,.F.);
#7388=ORIENTED_EDGE('',*,*,#5465,.F.);
#7389=ORIENTED_EDGE('',*,*,#5462,.F.);
#7390=ORIENTED_EDGE('',*,*,#5458,.F.);
#7391=ORIENTED_EDGE('',*,*,#5475,.F.);
#7392=ORIENTED_EDGE('',*,*,#5460,.F.);
#7393=ORIENTED_EDGE('',*,*,#5464,.F.);
#7394=ORIENTED_EDGE('',*,*,#5467,.F.);
#7395=ORIENTED_EDGE('',*,*,#5470,.F.);
#7396=ORIENTED_EDGE('',*,*,#5473,.F.);
#7397=ORIENTED_EDGE('',*,*,#5476,.F.);
#7398=ORIENTED_EDGE('',*,*,#5477,.F.);
#7399=ORIENTED_EDGE('',*,*,#5478,.F.);
#7400=ORIENTED_EDGE('',*,*,#5479,.T.);
#7401=ORIENTED_EDGE('',*,*,#5477,.T.);
#7402=ORIENTED_EDGE('',*,*,#5479,.F.);
#7403=ORIENTED_EDGE('',*,*,#5480,.F.);
#7404=ORIENTED_EDGE('',*,*,#5481,.T.);
#7405=ORIENTED_EDGE('',*,*,#5478,.T.);
#7406=ORIENTED_EDGE('',*,*,#5481,.F.);
#7407=ORIENTED_EDGE('',*,*,#5482,.F.);
#7408=ORIENTED_EDGE('',*,*,#5483,.T.);
#7409=ORIENTED_EDGE('',*,*,#5480,.T.);
#7410=ORIENTED_EDGE('',*,*,#5483,.F.);
#7411=ORIENTED_EDGE('',*,*,#5482,.T.);
#7412=ORIENTED_EDGE('',*,*,#5484,.F.);
#7413=ORIENTED_EDGE('',*,*,#5485,.F.);
#7414=ORIENTED_EDGE('',*,*,#5486,.T.);
#7415=ORIENTED_EDGE('',*,*,#5484,.T.);
#7416=ORIENTED_EDGE('',*,*,#5486,.F.);
#7417=ORIENTED_EDGE('',*,*,#5476,.T.);
#7418=ORIENTED_EDGE('',*,*,#5487,.T.);
#7419=ORIENTED_EDGE('',*,*,#5485,.T.);
#7420=ORIENTED_EDGE('',*,*,#5487,.F.);
#8105=CYLINDRICAL_SURFACE('',#9312,0.425);
#8106=CYLINDRICAL_SURFACE('',#9320,0.24505);
#8425=ADVANCED_FACE('',(#1131),#725,.F.);
#8426=ADVANCED_FACE('',(#1132),#726,.F.);
#8427=ADVANCED_FACE('',(#1133),#727,.F.);
#8428=ADVANCED_FACE('',(#1134),#728,.F.);
#8429=ADVANCED_FACE('',(#1135),#729,.F.);
#8430=ADVANCED_FACE('',(#1136),#730,.F.);
#8431=ADVANCED_FACE('',(#1137),#731,.F.);
#8432=ADVANCED_FACE('',(#1138),#732,.F.);
#8433=ADVANCED_FACE('',(#1139),#733,.F.);
#8434=ADVANCED_FACE('',(#1140),#734,.T.);
#8435=ADVANCED_FACE('',(#1141),#243,.T.);
#8436=ADVANCED_FACE('',(#1142),#8105,.T.);
#8437=ADVANCED_FACE('',(#1143),#244,.T.);
#8438=ADVANCED_FACE('',(#1144,#437),#735,.T.);
#8439=ADVANCED_FACE('',(#1145),#245,.T.);
#8440=ADVANCED_FACE('',(#1146),#8106,.T.);
#8602=CLOSED_SHELL('',(#8425,#8426,#8427,#8428,#8429,#8430,#8431,#8432));
#8603=CLOSED_SHELL('',(#8433,#8434,#8435,#8436,#8437,#8438,#8439,#8440));
#9297=AXIS2_PLACEMENT_3D('',#13592,#11079,#11080);
#9298=AXIS2_PLACEMENT_3D('',#13593,#11081,#11082);
#9299=AXIS2_PLACEMENT_3D('',#13602,#11087,#11088);
#9300=AXIS2_PLACEMENT_3D('',#13608,#11092,#11093);
#9301=AXIS2_PLACEMENT_3D('',#13614,#11097,#11098);
#9302=AXIS2_PLACEMENT_3D('',#13620,#11102,#11103);
#9303=AXIS2_PLACEMENT_3D('',#13626,#11107,#11108);
#9304=AXIS2_PLACEMENT_3D('',#13629,#11111,#11112);
#9305=AXIS2_PLACEMENT_3D('',#13630,#11113,#11114);
#9306=AXIS2_PLACEMENT_3D('',#13631,#11115,#11116);
#9307=AXIS2_PLACEMENT_3D('',#13633,#11117,#11118);
#9308=AXIS2_PLACEMENT_3D('',#13634,#11119,#11120);
#9309=AXIS2_PLACEMENT_3D('',#13636,#11121,#11122);
#9310=AXIS2_PLACEMENT_3D('',#13637,#11123,#11124);
#9311=AXIS2_PLACEMENT_3D('',#13639,#11125,#11126);
#9312=AXIS2_PLACEMENT_3D('',#13641,#11128,#11129);
#9313=AXIS2_PLACEMENT_3D('',#13643,#11130,#11131);
#9314=AXIS2_PLACEMENT_3D('',#13645,#11133,#11134);
#9315=AXIS2_PLACEMENT_3D('',#13647,#11135,#11136);
#9316=AXIS2_PLACEMENT_3D('',#13649,#11138,#11139);
#9317=AXIS2_PLACEMENT_3D('',#13651,#11140,#11141);
#9318=AXIS2_PLACEMENT_3D('',#13652,#11142,#11143);
#9319=AXIS2_PLACEMENT_3D('',#13654,#11144,#11145);
#9320=AXIS2_PLACEMENT_3D('',#13656,#11147,#11148);
#11079=DIRECTION('axis',(0.,0.,1.));
#11080=DIRECTION('refdir',(1.,0.,0.));
#11081=DIRECTION('center_axis',(0.866025403784439,0.,-0.5));
#11082=DIRECTION('ref_axis',(0.5,0.,0.866025403784439));
#11083=DIRECTION('',(-0.5,0.,-0.866025403784439));
#11084=DIRECTION('',(0.,-1.,0.));
#11085=DIRECTION('',(0.5,0.,0.866025403784439));
#11086=DIRECTION('',(0.,-1.,0.));
#11087=DIRECTION('center_axis',(1.20185167898973E-16,0.,-1.));
#11088=DIRECTION('ref_axis',(1.,0.,1.20185167898973E-16));
#11089=DIRECTION('',(-1.,0.,-1.20185167898973E-16));
#11090=DIRECTION('',(0.,-1.,0.));
#11091=DIRECTION('',(1.,0.,1.20185167898973E-16));
#11092=DIRECTION('center_axis',(-0.866025403784439,0.,-0.5));
#11093=DIRECTION('ref_axis',(0.5,0.,-0.866025403784439));
#11094=DIRECTION('',(-0.5,0.,0.866025403784439));
#11095=DIRECTION('',(0.,-1.,0.));
#11096=DIRECTION('',(0.5,0.,-0.866025403784439));
#11097=DIRECTION('center_axis',(-0.866025403784439,0.,0.5));
#11098=DIRECTION('ref_axis',(-0.5,0.,-0.866025403784439));
#11099=DIRECTION('',(0.5,0.,0.866025403784439));
#11100=DIRECTION('',(0.,-1.,0.));
#11101=DIRECTION('',(-0.5,0.,-0.866025403784439));
#11102=DIRECTION('center_axis',(-2.40370335797945E-16,0.,1.));
#11103=DIRECTION('ref_axis',(-1.,0.,-2.40370335797945E-16));
#11104=DIRECTION('',(1.,0.,2.40370335797945E-16));
#11105=DIRECTION('',(0.,-1.,0.));
#11106=DIRECTION('',(-1.,0.,-2.40370335797945E-16));
#11107=DIRECTION('center_axis',(0.866025403784439,0.,0.5));
#11108=DIRECTION('ref_axis',(-0.5,0.,0.866025403784439));
#11109=DIRECTION('',(0.5,0.,-0.866025403784439));
#11110=DIRECTION('',(-0.5,0.,0.866025403784439));
#11111=DIRECTION('center_axis',(0.,1.,0.));
#11112=DIRECTION('ref_axis',(1.,0.,0.));
#11113=DIRECTION('center_axis',(0.,-1.,0.));
#11114=DIRECTION('ref_axis',(0.,0.,-1.));
#11115=DIRECTION('center_axis',(0.,1.,0.));
#11116=DIRECTION('ref_axis',(1.,0.,0.));
#11117=DIRECTION('center_axis',(0.,1.,0.));
#11118=DIRECTION('ref_axis',(1.,0.,0.));
#11119=DIRECTION('center_axis',(0.,1.,0.));
#11120=DIRECTION('ref_axis',(0.,0.,1.));
#11121=DIRECTION('center_axis',(0.,-1.,0.));
#11122=DIRECTION('ref_axis',(1.,0.,0.));
#11123=DIRECTION('center_axis',(0.,-1.,0.));
#11124=DIRECTION('ref_axis',(1.,0.,0.));
#11125=DIRECTION('center_axis',(0.,-1.,0.));
#11126=DIRECTION('ref_axis',(1.,0.,0.));
#11127=DIRECTION('',(0.707106781186548,0.707106781186547,8.65956056235493E-17));
#11128=DIRECTION('center_axis',(0.,-1.,0.));
#11129=DIRECTION('ref_axis',(1.,0.,0.));
#11130=DIRECTION('center_axis',(0.,-1.,0.));
#11131=DIRECTION('ref_axis',(1.,0.,0.));
#11132=DIRECTION('',(0.,1.,0.));
#11133=DIRECTION('center_axis',(0.,1.,0.));
#11134=DIRECTION('ref_axis',(1.,0.,0.));
#11135=DIRECTION('center_axis',(0.,-1.,0.));
#11136=DIRECTION('ref_axis',(1.,0.,0.));
#11137=DIRECTION('',(-0.707106781186547,0.707106781186548,-8.65956056235493E-17));
#11138=DIRECTION('center_axis',(0.,-1.,0.));
#11139=DIRECTION('ref_axis',(0.,0.,-1.));
#11140=DIRECTION('center_axis',(0.,-1.,0.));
#11141=DIRECTION('ref_axis',(1.,0.,0.));
#11142=DIRECTION('center_axis',(0.,1.,0.));
#11143=DIRECTION('ref_axis',(1.,0.,0.));
#11144=DIRECTION('center_axis',(0.,1.,0.));
#11145=DIRECTION('ref_axis',(1.,0.,0.));
#11146=DIRECTION('',(-0.447213595499958,0.894427190999916,-5.47678698264203E-17));
#11147=DIRECTION('center_axis',(0.,-1.,0.));
#11148=DIRECTION('ref_axis',(1.,0.,0.));
#11149=DIRECTION('',(0.,1.,0.));
#13592=CARTESIAN_POINT('',(0.,0.,0.));
#13593=CARTESIAN_POINT('Origin',(0.115470053837925,-0.5,-0.2));
#13594=CARTESIAN_POINT('',(0.23094010767585,-0.5,0.));
#13595=CARTESIAN_POINT('',(0.115470053837925,-0.5,-0.2));
#13596=CARTESIAN_POINT('',(0.23094010767585,-0.5,0.));
#13597=CARTESIAN_POINT('',(0.115470053837925,-0.8,-0.2));
#13598=CARTESIAN_POINT('',(0.115470053837925,-0.5,-0.2));
#13599=CARTESIAN_POINT('',(0.23094010767585,-0.8,0.));
#13600=CARTESIAN_POINT('',(0.23094010767585,-0.8,0.));
#13601=CARTESIAN_POINT('',(0.23094010767585,-0.5,0.));
#13602=CARTESIAN_POINT('Origin',(-0.115470053837925,-0.5,-0.2));
#13603=CARTESIAN_POINT('',(-0.115470053837925,-0.5,-0.2));
#13604=CARTESIAN_POINT('',(0.115470053837925,-0.5,-0.2));
#13605=CARTESIAN_POINT('',(-0.115470053837925,-0.8,-0.2));
#13606=CARTESIAN_POINT('',(-0.115470053837925,-0.5,-0.2));
#13607=CARTESIAN_POINT('',(0.115470053837925,-0.8,-0.2));
#13608=CARTESIAN_POINT('Origin',(-0.23094010767585,-0.5,-2.77555756156289E-17));
#13609=CARTESIAN_POINT('',(-0.23094010767585,-0.5,-2.82820063659975E-17));
#13610=CARTESIAN_POINT('',(-0.115470053837925,-0.5,-0.2));
#13611=CARTESIAN_POINT('',(-0.23094010767585,-0.8,-2.77555756156289E-17));
#13612=CARTESIAN_POINT('',(-0.23094010767585,-0.5,-2.82820063659975E-17));
#13613=CARTESIAN_POINT('',(-0.115470053837925,-0.8,-0.2));
#13614=CARTESIAN_POINT('Origin',(-0.115470053837925,-0.5,0.2));
#13615=CARTESIAN_POINT('',(-0.115470053837925,-0.5,0.2));
#13616=CARTESIAN_POINT('',(-0.23094010767585,-0.5,-2.82820063659975E-17));
#13617=CARTESIAN_POINT('',(-0.115470053837925,-0.8,0.2));
#13618=CARTESIAN_POINT('',(-0.115470053837925,-0.5,0.2));
#13619=CARTESIAN_POINT('',(-0.23094010767585,-0.8,-2.82820063659975E-17));
#13620=CARTESIAN_POINT('Origin',(0.115470053837925,-0.5,0.2));
#13621=CARTESIAN_POINT('',(0.115470053837925,-0.5,0.2));
#13622=CARTESIAN_POINT('',(-0.115470053837925,-0.5,0.2));
#13623=CARTESIAN_POINT('',(0.115470053837925,-0.8,0.2));
#13624=CARTESIAN_POINT('',(0.115470053837925,-0.5,0.2));
#13625=CARTESIAN_POINT('',(-0.115470053837925,-0.8,0.2));
#13626=CARTESIAN_POINT('Origin',(0.23094010767585,-0.5,0.));
#13627=CARTESIAN_POINT('',(0.115470053837925,-0.5,0.2));
#13628=CARTESIAN_POINT('',(0.115470053837925,-0.8,0.2));
#13629=CARTESIAN_POINT('Origin',(0.,-0.5,0.));
#13630=CARTESIAN_POINT('Origin',(0.,-0.8,0.));
#13631=CARTESIAN_POINT('Origin',(0.,-1.4,0.));
#13632=CARTESIAN_POINT('',(-0.24505,-1.4,3.00099698131059E-17));
#13633=CARTESIAN_POINT('Origin',(0.,-1.4,0.));
#13634=CARTESIAN_POINT('Origin',(0.375,0.5,0.));
#13635=CARTESIAN_POINT('',(-0.375,0.5,-4.59242549680257E-17));
#13636=CARTESIAN_POINT('Origin',(0.,0.5,0.));
#13637=CARTESIAN_POINT('Origin',(0.,0.475,0.));
#13638=CARTESIAN_POINT('',(-0.425,0.45,-5.20474889637625E-17));
#13639=CARTESIAN_POINT('Origin',(0.,0.45,0.));
#13640=CARTESIAN_POINT('',(-0.4,0.475,-4.89858719658941E-17));
#13641=CARTESIAN_POINT('Origin',(0.,0.24,0.));
#13642=CARTESIAN_POINT('',(-0.425,0.0299999999999998,-5.20474889637625E-17));
#13643=CARTESIAN_POINT('Origin',(0.,0.0299999999999998,0.));
#13644=CARTESIAN_POINT('',(-0.425,0.24,-5.20474889637625E-17));
#13645=CARTESIAN_POINT('Origin',(0.,0.0150000000000001,0.));
#13646=CARTESIAN_POINT('',(-0.395,4.85722573273506E-17,-4.83735485663204E-17));
#13647=CARTESIAN_POINT('Origin',(0.,0.,0.));
#13648=CARTESIAN_POINT('',(-0.41,0.0150000000000001,-5.02105187650415E-17));
#13649=CARTESIAN_POINT('Origin',(0.27,0.,0.));
#13650=CARTESIAN_POINT('',(-0.27,0.,-3.30654635769785E-17));
#13651=CARTESIAN_POINT('Origin',(0.,0.,0.));
#13652=CARTESIAN_POINT('Origin',(0.,-0.02,0.));
#13653=CARTESIAN_POINT('',(-0.24505,-0.0498999999999999,3.00099698131059E-17));
#13654=CARTESIAN_POINT('Origin',(0.,-0.0498999999999999,0.));
#13655=CARTESIAN_POINT('',(-0.26,-0.02,-3.18408167778312E-17));
#13656=CARTESIAN_POINT('Origin',(0.,-0.995,0.));
#13657=CARTESIAN_POINT('',(-0.24505,-0.995,-3.00099698131059E-17));
#14430=UNCERTAINTY_MEASURE_WITH_UNIT(LENGTH_MEASURE(0.001),#14479,
'DISTANCE_ACCURACY_VALUE',
'Maximum model space distance between geometric entities at asserted c
onnectivities');
#14446=UNCERTAINTY_MEASURE_WITH_UNIT(LENGTH_MEASURE(0.001),#14479,
'DISTANCE_ACCURACY_VALUE',
'Maximum model space distance between geometric entities at asserted c
onnectivities');
#14462=(
GEOMETRIC_REPRESENTATION_CONTEXT(3)
GLOBAL_UNCERTAINTY_ASSIGNED_CONTEXT((#14430))
GLOBAL_UNIT_ASSIGNED_CONTEXT((#14479,#14481,#14482))
REPRESENTATION_CONTEXT('','3D')
);
#14478=(
GEOMETRIC_REPRESENTATION_CONTEXT(3)
GLOBAL_UNCERTAINTY_ASSIGNED_CONTEXT((#14446))
GLOBAL_UNIT_ASSIGNED_CONTEXT((#14479,#14481,#14482))
REPRESENTATION_CONTEXT('','3D')
);
#14479=(
LENGTH_UNIT()
NAMED_UNIT(*)
SI_UNIT(.CENTI.,.METRE.)
);
#14481=(
NAMED_UNIT(*)
PLANE_ANGLE_UNIT()
SI_UNIT($,.RADIAN.)
);
#14482=(
NAMED_UNIT(*)
SI_UNIT($,.STERADIAN.)
SOLID_ANGLE_UNIT()
);
#14498=SHAPE_DEFINITION_REPRESENTATION(#14529,#14618);
#14529=PRODUCT_DEFINITION_SHAPE('',$,#14650);
#14618=SHAPE_REPRESENTATION('',(#9297),#14462);
#14634=PRODUCT_DEFINITION_CONTEXT('part definition',#14729,'design');
#14650=PRODUCT_DEFINITION('M5x14 Cap Screw','M5x14 Cap Screw',#14681,#14634);
#14681=PRODUCT_DEFINITION_FORMATION('',$,#14746);
#14729=APPLICATION_CONTEXT(
'Core Data for Automotive Mechanical Design Process');
#14730=PRODUCT_CONTEXT('part definition',#14729,'mechanical');
#14746=PRODUCT('M5x14 Cap Screw','M5x14 Cap Screw','M5x14 Cap Screw',(#14730));
#14832=COLOUR_RGB('Black',0.12,0.14,0.17);
#14833=FILL_AREA_STYLE_COLOUR('',#14832);
#14834=FILL_AREA_STYLE('',(#14833));
#14835=SURFACE_STYLE_FILL_AREA(#14834);
#14836=SURFACE_SIDE_STYLE('',(#14835));
#14837=SURFACE_STYLE_USAGE(.BOTH.,#14836);
#14838=PRESENTATION_STYLE_ASSIGNMENT((#14837));
ENDSEC;
END-ISO-10303-21;
